ISO-10303-21;
HEADER;
FILE_DESCRIPTION (('STEP AP214'),
    '1' );
FILE_NAME ('angular contact ball bearing_68_iso_ISO 15 ABB - 1760 - 38,SI,NC,38_68.step',
    '2026-10-23T05:12:30',
    ( '' ),
    ( '' ),
    'SwSTEP 2.0',
    'SolidWorks 2026',
    '' );
FILE_SCHEMA (( 'AUTOMOTIVE_DESIGN' ));
ENDSEC;

DATA;
#7=ORIENTED_EDGE ( 'NONE', *, *, #982, .F. ) ;
#13=CARTESIAN_POINT ( 'NONE',  ( 3.199999999999996181, 4.555686092828153507E-15, 37.19999999999999574 ) ) ;
#34=ORIENTED_EDGE ( 'NONE', *, *, #1918, .F. ) ;
#60=CIRCLE ( 'NONE', #2217, 35.25000000000000000 ) ;
#66=DIRECTION ( 'NONE',  ( 0.000000000000000000, 0.000000000000000000, -1.000000000000000000 ) ) ;
#69=ORIENTED_EDGE ( 'NONE', *, *, #6641, .F. ) ;
#73=AXIS2_PLACEMENT_3D ( 'NONE', #3371, #4109, #6565 ) ;
#78=ORIENTED_EDGE ( 'NONE', *, *, #2938, .F. ) ;
#85=LINE ( 'NONE', #6673, #727 ) ;
#129=ADVANCED_FACE ( 'NONE', ( #4716 ), #4423, .T. ) ;
#132=CARTESIAN_POINT ( 'NONE',  ( -20.63749999999999929, 0.000000000000000000, 0.000000000000000000 ) ) ;
#145=DIRECTION ( 'NONE',  ( 1.000000000000000000, 0.000000000000000000, 0.000000000000000000 ) ) ;
#147=VERTEX_POINT ( 'NONE', #4043 ) ;
#152=CARTESIAN_POINT ( 'NONE',  ( 0.3344772040064616925, 0.000000000000000000, 31.52499999999999858 ) ) ;
#153=CIRCLE ( 'NONE', #6952, 37.50000000000000000 ) ;
#158=AXIS2_PLACEMENT_3D ( 'NONE', #3282, #2691, #5085 ) ;
#184=ORIENTED_EDGE ( 'NONE', *, *, #6782, .F. ) ;
#187=ADVANCED_FACE ( 'NONE', ( #728, #6616 ), #2484, .T. ) ;
#199=CARTESIAN_POINT ( 'NONE',  ( -20.63749999999999574, 0.000000000000000000, 0.000000000000000000 ) ) ;
#222=ORIENTED_EDGE ( 'NONE', *, *, #6161, .T. ) ;
#229=ADVANCED_FACE ( 'NONE', ( #767 ), #4425, .T. ) ;
#235=CARTESIAN_POINT ( 'NONE',  ( -3.200000000000007727, 0.000000000000000000, 0.000000000000000000 ) ) ;
#254=ORIENTED_EDGE ( 'NONE', *, *, #7228, .T. ) ;
#273=CIRCLE ( 'NONE', #5186, 30.30000000000000071 ) ;
#280=EDGE_CURVE ( 'NONE', #719, #2423, #3235, .T. ) ;
#283=TOROIDAL_SURFACE ( 'NONE', #2189, 37.19999999999999574, 0.3000000000000007661 ) ;
#291=ORIENTED_EDGE ( 'NONE', *, *, #5808, .T. ) ;
#293=VERTEX_POINT ( 'NONE', #6097 ) ;
#313=ORIENTED_EDGE ( 'NONE', *, *, #3930, .F. ) ;
#321=DIRECTION ( 'NONE',  ( 1.000000000000000000, 0.000000000000000000, 0.000000000000000000 ) ) ;
#324=AXIS2_PLACEMENT_3D ( 'NONE', #2355, #6089, #6606 ) ;
#336=DIRECTION ( 'NONE',  ( 1.000000000000000000, 0.000000000000000000, 0.000000000000000000 ) ) ;
#339=SURFACE_STYLE_USAGE ( .BOTH. , #6499 ) ;
#343=ORIENTED_EDGE ( 'NONE', *, *, #565, .F. ) ;
#351=CIRCLE ( 'NONE', #3314, 2.250000000000001776 ) ;
#356=CARTESIAN_POINT ( 'NONE',  ( -20.63749999999999929, 0.000000000000000000, 0.000000000000000000 ) ) ;
#379=AXIS2_PLACEMENT_3D ( 'NONE', #3051, #1902, #6121 ) ;
#388=DIRECTION ( 'NONE',  ( 0.000000000000000000, -1.000000000000000000, 0.000000000000000000 ) ) ;
#401=CARTESIAN_POINT ( 'NONE',  ( 0.000000000000000000, 4.133182947122317561E-15, -33.75000000000000000 ) ) ;
#420=SHAPE_REPRESENTATION ( 'angular contact ball bearing_68_iso_ISO 15 ABB - 1760 - 38,SI,NC,38_68', ( #7485 ), #6116 ) ;
#432=ORIENTED_EDGE ( 'NONE', *, *, #905, .T. ) ;
#435=CARTESIAN_POINT ( 'NONE',  ( 0.3344772040064616925, 0.000000000000000000, 0.000000000000000000 ) ) ;
#456=FILL_AREA_STYLE ('',( #4564 ) ) ;
#461=ORIENTED_EDGE ( 'NONE', *, *, #895, .F. ) ;
#471=ADVANCED_FACE ( 'NONE', ( #4987 ), #1329, .T. ) ;
#477=LINE ( 'NONE', #2186, #2610 ) ;
#482=ORIENTED_EDGE ( 'NONE', *, *, #5916, .F. ) ;
#521=ADVANCED_FACE ( 'NONE', ( #3486 ), #1713, .F. ) ;
#523=LINE ( 'NONE', #6483, #1208 ) ;
#534=ORIENTED_EDGE ( 'NONE', *, *, #2929, .F. ) ;
#549=DIRECTION ( 'NONE',  ( 1.000000000000000000, 0.000000000000000000, 0.000000000000000000 ) ) ;
#552=AXIS2_PLACEMENT_3D ( 'NONE', #3996, #7623, #7504 ) ;
#562=EDGE_CURVE ( 'NONE', #1095, #2283, #523, .T. ) ;
#563=ORIENTED_EDGE ( 'NONE', *, *, #6161, .F. ) ;
#564=VECTOR ( 'NONE', #809, 1000.000000000000000 ) ;
#565=EDGE_CURVE ( 'NONE', #2154, #3857, #3355, .T. ) ;
#568=CARTESIAN_POINT ( 'NONE',  ( -1.677050983124841466, 3.949485927250214050E-15, 32.25000000000000000 ) ) ;
#571=DIRECTION ( 'NONE',  ( 0.000000000000000000, 0.000000000000000000, -1.000000000000000000 ) ) ;
#601=EDGE_CURVE ( 'NONE', #3231, #6794, #5455, .T. ) ;
#605=ADVANCED_FACE ( 'NONE', ( #1152 ), #4305, .T. ) ;
#612=AXIS2_PLACEMENT_3D ( 'NONE', #3104, #6064, #4946 ) ;
#616=EDGE_CURVE ( 'NONE', #7044, #7003, #5625, .T. ) ;
#619=CARTESIAN_POINT ( 'NONE',  ( 0.3344772040064616925, 0.000000000000000000, 0.000000000000000000 ) ) ;
#650=ORIENTED_EDGE ( 'NONE', *, *, #4418, .F. ) ;
#661=ORIENTED_EDGE ( 'NONE', *, *, #6270, .T. ) ;
#688=VERTEX_POINT ( 'NONE', #568 ) ;
#719=VERTEX_POINT ( 'NONE', #2731 ) ;
#720=DIRECTION ( 'NONE',  ( 0.000000000000000000, 0.000000000000000000, -1.000000000000000000 ) ) ;
#727=VECTOR ( 'NONE', #7229, 1000.000000000000000 ) ;
#728=FACE_BOUND ( 'NONE', #6470, .T. ) ;
#729=CARTESIAN_POINT ( 'NONE',  ( -3.499999999999996447, 35.97500000000000142, 0.000000000000000000 ) ) ;
#738=VERTEX_POINT ( 'NONE', #5093 ) ;
#741=( NAMED_UNIT ( * ) SI_UNIT ( $, .STERADIAN. ) SOLID_ANGLE_UNIT ( ) );
#767=FACE_OUTER_BOUND ( 'NONE', #7254, .T. ) ;
#769=DIRECTION ( 'NONE',  ( 0.000000000000000000, 1.000000000000000000, -1.224646799147353207E-16 ) ) ;
#782=AXIS2_PLACEMENT_3D ( 'NONE', #13, #2471, #1266 ) ;
#791=CARTESIAN_POINT ( 'NONE',  ( -3.499999999999996003, 0.000000000000000000, 0.000000000000000000 ) ) ;
#807=CIRCLE ( 'NONE', #7607, 31.52499999999999858 ) ;
#809=DIRECTION ( 'NONE',  ( 1.000000000000000000, 0.000000000000000000, 0.000000000000000000 ) ) ;
#817=APPLICATION_CONTEXT ( 'automotive_design' ) ;
#834=CARTESIAN_POINT ( 'NONE',  ( 0.000000000000000000, 0.000000000000000000, 0.000000000000000000 ) ) ;
#862=ADVANCED_FACE ( 'NONE', ( #5018 ), #5492, .T. ) ;
#867=ORIENTED_EDGE ( 'NONE', *, *, #6490, .T. ) ;
#868=VECTOR ( 'NONE', #5469, 1000.000000000000000 ) ;
#895=EDGE_CURVE ( 'NONE', #6664, #1974, #7265, .T. ) ;
#896=ORIENTED_EDGE ( 'NONE', *, *, #1918, .T. ) ;
#902=DIRECTION ( 'NONE',  ( 1.000000000000000000, 0.000000000000000000, 0.000000000000000000 ) ) ;
#905=EDGE_CURVE ( 'NONE', #5391, #738, #477, .T. ) ;
#908=CYLINDRICAL_SURFACE ( 'NONE', #3452, 30.00000000000000000 ) ;
#937=ORIENTED_EDGE ( 'NONE', *, *, #5766, .F. ) ;
#966=CARTESIAN_POINT ( 'NONE',  ( 3.200000000000008171, 0.000000000000000000, 0.000000000000000000 ) ) ;
#975=CARTESIAN_POINT ( 'NONE',  ( 0.000000000000000000, 0.000000000000000000, 0.000000000000000000 ) ) ;
#978=AXIS2_PLACEMENT_3D ( 'NONE', #4718, #5233, #4007 ) ;
#982=EDGE_CURVE ( 'NONE', #7003, #6794, #4107, .T. ) ;
#996=CARTESIAN_POINT ( 'NONE',  ( -3.200000000000008171, 0.000000000000000000, 0.000000000000000000 ) ) ;
#997=EDGE_CURVE ( 'NONE', #4531, #688, #3115, .T. ) ;
#1052=ADVANCED_BREP_SHAPE_REPRESENTATION ( '', ( #5741, #7485 ), #6116 ) ;
#1074=DIRECTION ( 'NONE',  ( 1.000000000000000000, 0.000000000000000000, 0.000000000000000000 ) ) ;
#1088=DIRECTION ( 'NONE',  ( 1.000000000000000000, 0.000000000000000000, 0.000000000000000000 ) ) ;
#1094=ORIENTED_EDGE ( 'NONE', *, *, #3440, .F. ) ;
#1095=VERTEX_POINT ( 'NONE', #7429 ) ;
#1103=AXIS2_PLACEMENT_3D ( 'NONE', #5937, #2278, #2945 ) ;
#1107=CARTESIAN_POINT ( 'NONE',  ( 3.500000000000006661, 0.000000000000000000, -31.52499999999999858 ) ) ;
#1113=FACE_OUTER_BOUND ( 'NONE', #4887, .T. ) ;
#1114=DIRECTION ( 'NONE',  ( 0.000000000000000000, 0.000000000000000000, -1.000000000000000000 ) ) ;
#1116=CARTESIAN_POINT ( 'NONE',  ( -3.500000000000007550, 0.000000000000000000, -30.30000000000000071 ) ) ;
#1144=ADVANCED_FACE ( 'NONE', ( #1961 ), #1597, .T. ) ;
#1152=FACE_OUTER_BOUND ( 'NONE', #1692, .T. ) ;
#1180=ORIENTED_EDGE ( 'NONE', *, *, #4758, .F. ) ;
#1184=EDGE_CURVE ( 'NONE', #1401, #5872, #5501, .T. ) ;
#1195=PRODUCT_DEFINITION_SHAPE ( 'NONE', 'NONE',  #7059 ) ;
#1197=DIRECTION ( 'NONE',  ( 0.000000000000000000, 0.000000000000000000, -1.000000000000000000 ) ) ;
#1208=VECTOR ( 'NONE', #1074, 1000.000000000000000 ) ;
#1209=( NAMED_UNIT ( * ) SI_UNIT ( $, .STERADIAN. ) SOLID_ANGLE_UNIT ( ) );
#1213=VECTOR ( 'NONE', #2509, 1000.000000000000000 ) ;
#1218=AXIS2_PLACEMENT_3D ( 'NONE', #5252, #388, #6471 ) ;
#1247=DIRECTION ( 'NONE',  ( 0.000000000000000000, 0.000000000000000000, -1.000000000000000000 ) ) ;
#1253=EDGE_LOOP ( 'NONE', ( #3710, #461 ) ) ;
#1266=DIRECTION ( 'NONE',  ( 0.000000000000000000, 1.224646799147359124E-16, 1.000000000000000000 ) ) ;
#1271=DIRECTION ( 'NONE',  ( 1.000000000000000000, 0.000000000000000000, 0.000000000000000000 ) ) ;
#1279=DIRECTION ( 'NONE',  ( 1.000000000000000000, 0.000000000000000000, 0.000000000000000000 ) ) ;
#1284=( NAMED_UNIT ( * ) PLANE_ANGLE_UNIT ( ) SI_UNIT ( $, .RADIAN. ) );
#1286=CARTESIAN_POINT ( 'NONE',  ( 3.500000000000007550, 3.710679801416480038E-15, 30.30000000000000071 ) ) ;
#1299=CIRCLE ( 'NONE', #4697, 0.3000000000000016542 ) ;
#1301=CARTESIAN_POINT ( 'NONE',  ( 0.000000000000000000, 0.000000000000000000, 0.000000000000000000 ) ) ;
#1329=TOROIDAL_SURFACE ( 'NONE', #5369, 30.30000000000000071, 0.3000000000000003775 ) ;
#1353=ORIENTED_EDGE ( 'NONE', *, *, #7213, .T. ) ;
#1399=CARTESIAN_POINT ( 'NONE',  ( -3.499999999999996003, 4.574055794815363937E-15, 37.19999999999999574 ) ) ;
#1401=VERTEX_POINT ( 'NONE', #4164 ) ;
#1416=DIRECTION ( 'NONE',  ( 0.000000000000000000, 0.000000000000000000, -1.000000000000000000 ) ) ;
#1418=ORIENTED_EDGE ( 'NONE', *, *, #1826, .T. ) ;
#1419=ADVANCED_FACE ( 'NONE', ( #6619 ), #3461, .F. ) ;
#1441=ORIENTED_EDGE ( 'NONE', *, *, #5678, .F. ) ;
#1448=DIRECTION ( 'NONE',  ( -1.000000000000000000, -0.000000000000000000, -0.000000000000000000 ) ) ;
#1456=PRODUCT_DEFINITION_CONTEXT ( 'detailed design', #817, 'design' ) ;
#1464=ADVANCED_FACE ( 'NONE', ( #5356 ), #7645, .T. ) ;
#1496=VERTEX_POINT ( 'NONE', #3106 ) ;
#1583=EDGE_CURVE ( 'NONE', #5377, #1095, #3495, .T. ) ;
#1597=TOROIDAL_SURFACE ( 'NONE', #2369, 37.19999999999999574, 0.3000000000000007661 ) ;
#1613=DIRECTION ( 'NONE',  ( -1.000000000000000000, -0.000000000000000000, -0.000000000000000000 ) ) ;
#1622=DIRECTION ( 'NONE',  ( 0.000000000000000000, 0.000000000000000000, -1.000000000000000000 ) ) ;
#1634=DIRECTION ( 'NONE',  ( 0.000000000000000000, 0.000000000000000000, -1.000000000000000000 ) ) ;
#1645=CARTESIAN_POINT ( 'NONE',  ( 0.000000000000000000, 0.000000000000000000, 0.000000000000000000 ) ) ;
#1665=CARTESIAN_POINT ( 'NONE',  ( -20.63749999999999929, 0.000000000000000000, 0.000000000000000000 ) ) ;
#1681=VECTOR ( 'NONE', #4745, 1000.000000000000000 ) ;
#1692=EDGE_LOOP ( 'NONE', ( #3302, #4764, #4390, #7015 ) ) ;
#1713=CYLINDRICAL_SURFACE ( 'NONE', #73, 35.25000000000000000 ) ;
#1739=AXIS2_PLACEMENT_3D ( 'NONE', #1645, #4123, #2834 ) ;
#1740=ORIENTED_EDGE ( 'NONE', *, *, #6270, .F. ) ;
#1748=AXIS2_PLACEMENT_3D ( 'NONE', #7742, #5385, #2241 ) ;
#1762=CARTESIAN_POINT ( 'NONE',  ( -20.63749999999999929, 0.000000000000000000, 0.000000000000000000 ) ) ;
#1773=PLANE ( 'NONE',  #4137 ) ;
#1798=DIRECTION ( 'NONE',  ( 1.000000000000000000, 0.000000000000000000, 0.000000000000000000 ) ) ;
#1805=EDGE_LOOP ( 'NONE', ( #7004, #6633, #7255, #3673 ) ) ;
#1813=AXIS2_PLACEMENT_3D ( 'NONE', #2584, #1271, #3723 ) ;
#1826=EDGE_CURVE ( 'NONE', #6698, #5437, #6525, .T. ) ;
#1841=CARTESIAN_POINT ( 'NONE',  ( -3.500000000000006661, 0.000000000000000000, -32.25000000000000000 ) ) ;
#1844=CARTESIAN_POINT ( 'NONE',  ( -3.500000000000006661, 0.000000000000000000, 0.000000000000000000 ) ) ;
#1852=CARTESIAN_POINT ( 'NONE',  ( 3.500000000000007550, 0.000000000000000000, -30.30000000000000071 ) ) ;
#1853=ORIENTED_EDGE ( 'NONE', *, *, #4625, .T. ) ;
#1869=EDGE_CURVE ( 'NONE', #3231, #2154, #2875, .T. ) ;
#1872=ORIENTED_EDGE ( 'NONE', *, *, #7071, .T. ) ;
#1875=TOROIDAL_SURFACE ( 'NONE', #3766, 30.30000000000000071, 0.3000000000000003775 ) ;
#1877=LINE ( 'NONE', #4905, #4756 ) ;
#1894=DIRECTION ( 'NONE',  ( 0.000000000000000000, 0.000000000000000000, -1.000000000000000000 ) ) ;
#1902=DIRECTION ( 'NONE',  ( 1.000000000000000000, 0.000000000000000000, 0.000000000000000000 ) ) ;
#1907=VERTEX_POINT ( 'NONE', #1116 ) ;
#1914=EDGE_CURVE ( 'NONE', #7003, #7044, #2622, .T. ) ;
#1918=EDGE_CURVE ( 'NONE', #6794, #5950, #3755, .T. ) ;
#1919=DIRECTION ( 'NONE',  ( 0.000000000000000000, 0.000000000000000000, 1.000000000000000000 ) ) ;
#1922=DIRECTION ( 'NONE',  ( 0.000000000000000000, -1.224646799147352961E-16, 1.000000000000000000 ) ) ;
#1927=DIRECTION ( 'NONE',  ( 0.000000000000000000, 0.000000000000000000, -1.000000000000000000 ) ) ;
#1949=CIRCLE ( 'NONE', #6101, 35.97500000000000142 ) ;
#1961=FACE_OUTER_BOUND ( 'NONE', #7585, .T. ) ;
#1974=VERTEX_POINT ( 'NONE', #1841 ) ;
#1976=EDGE_LOOP ( 'NONE', ( #3215, #1853, #5616, #5995 ) ) ;
#1990=CARTESIAN_POINT ( 'NONE',  ( -3.200000000000007727, 0.000000000000000000, -30.30000000000000071 ) ) ;
#1996=AXIS2_PLACEMENT_3D ( 'NONE', #2323, #6569, #571 ) ;
#2001=CARTESIAN_POINT ( 'NONE',  ( -3.200000000000007727, 0.000000000000000000, 0.000000000000000000 ) ) ;
#2004=AXIS2_PLACEMENT_3D ( 'NONE', #4562, #7128, #2833 ) ;
#2006=DIRECTION ( 'NONE',  ( 1.000000000000000000, 0.000000000000000000, 0.000000000000000000 ) ) ;
#2025=EDGE_CURVE ( 'NONE', #5644, #2609, #1877, .T. ) ;
#2027=DIRECTION ( 'NONE',  ( 0.000000000000000000, 0.000000000000000000, -1.000000000000000000 ) ) ;
#2068=EDGE_CURVE ( 'NONE', #5644, #5391, #5127, .T. ) ;
#2136=TOROIDAL_SURFACE ( 'NONE', #7290, 30.30000000000000071, 0.3000000000000003775 ) ;
#2153=DIRECTION ( 'NONE',  ( 1.000000000000000000, 0.000000000000000000, 0.000000000000000000 ) ) ;
#2154=VERTEX_POINT ( 'NONE', #2733 ) ;
#2164=EDGE_LOOP ( 'NONE', ( #5033, #254, #1353, #2293 ) ) ;
#2165=ORIENTED_EDGE ( 'NONE', *, *, #2938, .T. ) ;
#2169=FACE_OUTER_BOUND ( 'NONE', #5325, .T. ) ;
#2178=LINE ( 'NONE', #5161, #4292 ) ;
#2179=ADVANCED_FACE ( 'NONE', ( #5131 ), #2136, .T. ) ;
#2186=CARTESIAN_POINT ( 'NONE',  ( -20.63749999999999574, 4.592425496802574367E-15, 37.50000000000000000 ) ) ;
#2187=CARTESIAN_POINT ( 'NONE',  ( 3.500000000000006661, 3.860699034312030436E-15, 31.52499999999999858 ) ) ;
#2189=AXIS2_PLACEMENT_3D ( 'NONE', #6607, #4561, #1197 ) ;
#2202=AXIS2_PLACEMENT_3D ( 'NONE', #6764, #2550, #4937 ) ;
#2207=DIRECTION ( 'NONE',  ( 1.000000000000000000, 0.000000000000000000, 0.000000000000000000 ) ) ;
#2208=AXIS2_PLACEMENT_3D ( 'NONE', #2239, #4630, #1634 ) ;
#2217=AXIS2_PLACEMENT_3D ( 'NONE', #4158, #2985, #6721 ) ;
#2222=FACE_OUTER_BOUND ( 'NONE', #4382, .T. ) ;
#2233=DIRECTION ( 'NONE',  ( 1.000000000000000000, 0.000000000000000000, 0.000000000000000000 ) ) ;
#2236=AXIS2_PLACEMENT_3D ( 'NONE', #3018, #1798, #720 ) ;
#2239=CARTESIAN_POINT ( 'NONE',  ( -20.63749999999999574, 0.000000000000000000, 0.000000000000000000 ) ) ;
#2241=DIRECTION ( 'NONE',  ( 0.000000000000000000, 0.000000000000000000, -1.000000000000000000 ) ) ;
#2261=AXIS2_PLACEMENT_3D ( 'NONE', #6691, #2485, #1927 ) ;
#2270=EDGE_LOOP ( 'NONE', ( #2712, #7610, #6037, #896 ) ) ;
#2272=ORIENTED_EDGE ( 'NONE', *, *, #5766, .T. ) ;
#2278=DIRECTION ( 'NONE',  ( 1.000000000000000000, 0.000000000000000000, 0.000000000000000000 ) ) ;
#2283=VERTEX_POINT ( 'NONE', #1107 ) ;
#2288=CARTESIAN_POINT ( 'NONE',  ( -20.63749999999999574, 0.000000000000000000, 0.000000000000000000 ) ) ;
#2289=PRESENTATION_STYLE_ASSIGNMENT (( #339 ) ) ;
#2291=DIRECTION ( 'NONE',  ( 1.000000000000000000, 0.000000000000000000, 0.000000000000000000 ) ) ;
#2293=ORIENTED_EDGE ( 'NONE', *, *, #601, .F. ) ;
#2297=ORIENTED_EDGE ( 'NONE', *, *, #4384, .F. ) ;
#2298=DIRECTION ( 'NONE',  ( 0.000000000000000000, 0.000000000000000000, -1.000000000000000000 ) ) ;
#2311=CARTESIAN_POINT ( 'NONE',  ( -20.63749999999999929, 3.860699034312030436E-15, 31.52499999999999858 ) ) ;
#2323=CARTESIAN_POINT ( 'NONE',  ( 3.499999999999996003, 0.000000000000000000, 0.000000000000000000 ) ) ;
#2344=CYLINDRICAL_SURFACE ( 'NONE', #7596, 30.00000000000000000 ) ;
#2355=CARTESIAN_POINT ( 'NONE',  ( -3.200000000000007727, 3.710679801416480038E-15, 30.30000000000000071 ) ) ;
#2367=CARTESIAN_POINT ( 'NONE',  ( 3.200000000000007727, 0.000000000000000000, 0.000000000000000000 ) ) ;
#2369=AXIS2_PLACEMENT_3D ( 'NONE', #4392, #3808, #5619 ) ;
#2376=AXIS2_PLACEMENT_3D ( 'NONE', #619, #4913, #4280 ) ;
#2387=CIRCLE ( 'NONE', #5269, 35.25000000000000000 ) ;
#2392=ORIENTED_EDGE ( 'NONE', *, *, #7691, .T. ) ;
#2393=CIRCLE ( 'NONE', #2004, 32.25000000000000000 ) ;
#2396=FACE_BOUND ( 'NONE', #3451, .T. ) ;
#2418=CARTESIAN_POINT ( 'NONE',  ( -3.500000000000006661, 0.000000000000000000, 0.000000000000000000 ) ) ;
#2421=DIRECTION ( 'NONE',  ( 0.000000000000000000, 0.000000000000000000, -1.000000000000000000 ) ) ;
#2423=VERTEX_POINT ( 'NONE', #2428 ) ;
#2428=CARTESIAN_POINT ( 'NONE',  ( 1.677050983124841466, 4.316879966994421072E-15, -35.25000000000000000 ) ) ;
#2433=CARTESIAN_POINT ( 'NONE',  ( -3.499999999999996003, 4.405666859932603897E-15, 35.97500000000000142 ) ) ;
#2443=CARTESIAN_POINT ( 'NONE',  ( 1.677050983124841466, 0.000000000000000000, 0.000000000000000000 ) ) ;
#2471=DIRECTION ( 'NONE',  ( 0.000000000000000000, 1.000000000000000000, -1.224646799147353207E-16 ) ) ;
#2484=PLANE ( 'NONE',  #5951 ) ;
#2485=DIRECTION ( 'NONE',  ( 1.000000000000000000, 0.000000000000000000, 0.000000000000000000 ) ) ;
#2494=ORIENTED_EDGE ( 'NONE', *, *, #4029, .F. ) ;
#2507=EDGE_CURVE ( 'NONE', #6664, #688, #85, .T. ) ;
#2509=DIRECTION ( 'NONE',  ( 1.000000000000000000, 0.000000000000000000, 0.000000000000000000 ) ) ;
#2514=UNCERTAINTY_MEASURE_WITH_UNIT (LENGTH_MEASURE( 1.000000000000000082E-05 ), #4283, 'distance_accuracy_value', 'NONE');
#2524=DIRECTION ( 'NONE',  ( 0.000000000000000000, 0.000000000000000000, -1.000000000000000000 ) ) ;
#2528=ORIENTED_EDGE ( 'NONE', *, *, #280, .F. ) ;
#2533=DIRECTION ( 'NONE',  ( 1.000000000000000000, 0.000000000000000000, 0.000000000000000000 ) ) ;
#2538=CIRCLE ( 'NONE', #7559, 31.52499999999999858 ) ;
#2546=ORIENTED_EDGE ( 'NONE', *, *, #1583, .F. ) ;
#2550=DIRECTION ( 'NONE',  ( -1.000000000000000000, -0.000000000000000000, -0.000000000000000000 ) ) ;
#2551=CARTESIAN_POINT ( 'NONE',  ( 3.499999999999996003, 37.19999999999999574, 0.000000000000000000 ) ) ;
#2555=CARTESIAN_POINT ( 'NONE',  ( 3.199999999999994404, 0.000000000000000000, 0.000000000000000000 ) ) ;
#2560=ADVANCED_FACE ( 'NONE', ( #5607 ), #1875, .T. ) ;
#2568=EDGE_CURVE ( 'NONE', #2609, #5437, #3458, .T. ) ;
#2584=CARTESIAN_POINT ( 'NONE',  ( 3.500000000000008438, 30.30000000000000071, 0.000000000000000000 ) ) ;
#2609=VERTEX_POINT ( 'NONE', #7052 ) ;
#2610=VECTOR ( 'NONE', #3363, 1000.000000000000000 ) ;
#2611=ORIENTED_EDGE ( 'NONE', *, *, #7401, .T. ) ;
#2616=DIRECTION ( 'NONE',  ( 1.000000000000000000, 0.000000000000000000, 0.000000000000000000 ) ) ;
#2622=CIRCLE ( 'NONE', #1748, 30.30000000000000071 ) ;
#2628=EDGE_CURVE ( 'NONE', #5377, #719, #351, .T. ) ;
#2647=ORIENTED_EDGE ( 'NONE', *, *, #562, .F. ) ;
#2654=CYLINDRICAL_SURFACE ( 'NONE', #4058, 35.97500000000000853 ) ;
#2660=AXIS2_PLACEMENT_3D ( 'NONE', #7683, #4133, #2298 ) ;
#2691=DIRECTION ( 'NONE',  ( 1.000000000000000000, 0.000000000000000000, 0.000000000000000000 ) ) ;
#2696=DIRECTION ( 'NONE',  ( 0.000000000000000000, 0.000000000000000000, -1.000000000000000000 ) ) ;
#2699=DIRECTION ( 'NONE',  ( 0.000000000000000000, 0.000000000000000000, -1.000000000000000000 ) ) ;
#2708=CIRCLE ( 'NONE', #3457, 2.250000000000001776 ) ;
#2712=ORIENTED_EDGE ( 'NONE', *, *, #7228, .F. ) ;
#2731=CARTESIAN_POINT ( 'NONE',  ( 1.677050983124841466, 0.000000000000000000, 35.25000000000000000 ) ) ;
#2733=CARTESIAN_POINT ( 'NONE',  ( -3.200000000000008171, 3.673940397442059178E-15, 30.00000000000000000 ) ) ;
#2754=LINE ( 'NONE', #5189, #1681 ) ;
#2775=DIRECTION ( 'NONE',  ( 0.000000000000000000, 0.000000000000000000, -1.000000000000000000 ) ) ;
#2802=ORIENTED_EDGE ( 'NONE', *, *, #616, .F. ) ;
#2805=PLANE ( 'NONE',  #7666 ) ;
#2808=VECTOR ( 'NONE', #4973, 1000.000000000000000 ) ;
#2833=DIRECTION ( 'NONE',  ( 0.000000000000000000, 0.000000000000000000, -1.000000000000000000 ) ) ;
#2834=DIRECTION ( 'NONE',  ( 0.000000000000000000, 0.000000000000000000, 1.000000000000000000 ) ) ;
#2836=FACE_OUTER_BOUND ( 'NONE', #1976, .T. ) ;
#2850=DIRECTION ( 'NONE',  ( 0.000000000000000000, 0.000000000000000000, 1.000000000000000000 ) ) ;
#2861=DIRECTION ( 'NONE',  ( 0.000000000000000000, 0.000000000000000000, -1.000000000000000000 ) ) ;
#2872=( NAMED_UNIT ( * ) PLANE_ANGLE_UNIT ( ) SI_UNIT ( $, .RADIAN. ) );
#2875=CIRCLE ( 'NONE', #7149, 30.00000000000000000 ) ;
#2929=EDGE_CURVE ( 'NONE', #719, #293, #7329, .T. ) ;
#2930=CARTESIAN_POINT ( 'NONE',  ( -3.500000000000006661, 0.000000000000000000, 0.000000000000000000 ) ) ;
#2931=DIRECTION ( 'NONE',  ( -1.000000000000000000, -0.000000000000000000, -0.000000000000000000 ) ) ;
#2938=EDGE_CURVE ( 'NONE', #147, #688, #4907, .T. ) ;
#2945=DIRECTION ( 'NONE',  ( 0.000000000000000000, 0.000000000000000000, -1.000000000000000000 ) ) ;
#2956=DIRECTION ( 'NONE',  ( 0.000000000000000000, 0.000000000000000000, -1.000000000000000000 ) ) ;
#2960=AXIS2_PLACEMENT_3D ( 'NONE', #791, #3210, #5532 ) ;
#2985=DIRECTION ( 'NONE',  ( 1.000000000000000000, 0.000000000000000000, 0.000000000000000000 ) ) ;
#2989=ADVANCED_FACE ( 'NONE', ( #3228 ), #7397, .T. ) ;
#3007=ORIENTED_EDGE ( 'NONE', *, *, #2568, .T. ) ;
#3018=CARTESIAN_POINT ( 'NONE',  ( 3.500000000000006661, 0.000000000000000000, 0.000000000000000000 ) ) ;
#3041=ORIENTED_EDGE ( 'NONE', *, *, #2568, .F. ) ;
#3051=CARTESIAN_POINT ( 'NONE',  ( 3.199999999999996181, 0.000000000000000000, 0.000000000000000000 ) ) ;
#3060=AXIS2_PLACEMENT_3D ( 'NONE', #2555, #4943, #2699 ) ;
#3069=CARTESIAN_POINT ( 'NONE',  ( -1.677050983124841466, 0.000000000000000000, 0.000000000000000000 ) ) ;
#3071=DIRECTION ( 'NONE',  ( 0.000000000000000000, 0.000000000000000000, -1.000000000000000000 ) ) ;
#3077=DIRECTION ( 'NONE',  ( 1.000000000000000000, 0.000000000000000000, 0.000000000000000000 ) ) ;
#3085=ORIENTED_EDGE ( 'NONE', *, *, #1583, .T. ) ;
#3104=CARTESIAN_POINT ( 'NONE',  ( 0.000000000000000000, 0.000000000000000000, 0.000000000000000000 ) ) ;
#3105=FACE_BOUND ( 'NONE', #7700, .T. ) ;
#3106=CARTESIAN_POINT ( 'NONE',  ( -0.3344772040064616925, 4.405666859932604686E-15, -35.97500000000000853 ) ) ;
#3115=CIRCLE ( 'NONE', #1218, 2.250000000000001776 ) ;
#3117=DIRECTION ( 'NONE',  ( 1.000000000000000000, 0.000000000000000000, 0.000000000000000000 ) ) ;
#3129=EDGE_CURVE ( 'NONE', #7232, #4531, #5407, .T. ) ;
#3132=VERTEX_POINT ( 'NONE', #6629 ) ;
#3149=SHAPE_DEFINITION_REPRESENTATION ( #1195, #420 ) ;
#3170=CIRCLE ( 'NONE', #7195, 30.30000000000000071 ) ;
#3196=AXIS2_PLACEMENT_3D ( 'NONE', #966, #336, #7739 ) ;
#3197=CARTESIAN_POINT ( 'NONE',  ( -3.200000000000008171, 0.000000000000000000, 0.000000000000000000 ) ) ;
#3204=TOROIDAL_SURFACE ( 'NONE', #4458, 37.19999999999999574, 0.3000000000000007661 ) ;
#3210=DIRECTION ( 'NONE',  ( 1.000000000000000000, 0.000000000000000000, 0.000000000000000000 ) ) ;
#3213=DIRECTION ( 'NONE',  ( 0.000000000000000000, 0.000000000000000000, -1.000000000000000000 ) ) ;
#3214=CIRCLE ( 'NONE', #7612, 32.25000000000000000 ) ;
#3215=ORIENTED_EDGE ( 'NONE', *, *, #1184, .T. ) ;
#3217=DIRECTION ( 'NONE',  ( 1.000000000000000000, 0.000000000000000000, 0.000000000000000000 ) ) ;
#3228=FACE_OUTER_BOUND ( 'NONE', #6706, .T. ) ;
#3231=VERTEX_POINT ( 'NONE', #5154 ) ;
#3235=CIRCLE ( 'NONE', #3704, 35.25000000000000000 ) ;
#3246=AXIS2_PLACEMENT_3D ( 'NONE', #2288, #1088, #3499 ) ;
#3249=CARTESIAN_POINT ( 'NONE',  ( 3.200000000000007727, 0.000000000000000000, 0.000000000000000000 ) ) ;
#3251=CARTESIAN_POINT ( 'NONE',  ( -3.199999999999994404, 0.000000000000000000, 0.000000000000000000 ) ) ;
#3282=CARTESIAN_POINT ( 'NONE',  ( -3.499999999999996003, 0.000000000000000000, 0.000000000000000000 ) ) ;
#3302=ORIENTED_EDGE ( 'NONE', *, *, #2507, .F. ) ;
#3314=AXIS2_PLACEMENT_3D ( 'NONE', #5083, #7380, #2027 ) ;
#3337=AXIS2_PLACEMENT_3D ( 'NONE', #4154, #6122, #1114 ) ;
#3355=CIRCLE ( 'NONE', #324, 0.3000000000000016542 ) ;
#3363=DIRECTION ( 'NONE',  ( 1.000000000000000000, 0.000000000000000000, 0.000000000000000000 ) ) ;
#3371=CARTESIAN_POINT ( 'NONE',  ( -20.63749999999999574, 0.000000000000000000, 0.000000000000000000 ) ) ;
#3383=CIRCLE ( 'NONE', #5403, 0.3000000000000016542 ) ;
#3386=SURFACE_STYLE_FILL_AREA ( #456 ) ;
#3404=CYLINDRICAL_SURFACE ( 'NONE', #4934, 32.25000000000000000 ) ;
#3409=CYLINDRICAL_SURFACE ( 'NONE', #2208, 37.50000000000000000 ) ;
#3414=TOROIDAL_SURFACE ( 'NONE', #5045, 33.75000000000000000, 2.250000000000000444 ) ;
#3426=ORIENTED_EDGE ( 'NONE', *, *, #6398, .F. ) ;
#3432=CIRCLE ( 'NONE', #158, 35.97500000000000142 ) ;
#3434=DIRECTION ( 'NONE',  ( 1.000000000000000000, 0.000000000000000000, 0.000000000000000000 ) ) ;
#3440=EDGE_CURVE ( 'NONE', #1095, #5377, #2538, .T. ) ;
#3451=EDGE_LOOP ( 'NONE', ( #6176, #2802 ) ) ;
#3452=AXIS2_PLACEMENT_3D ( 'NONE', #356, #5686, #2696 ) ;
#3457=AXIS2_PLACEMENT_3D ( 'NONE', #6731, #3693, #1922 ) ;
#3458=CIRCLE ( 'NONE', #3337, 0.3000000000000016542 ) ;
#3461=CYLINDRICAL_SURFACE ( 'NONE', #3246, 35.25000000000000000 ) ;
#3462=( LENGTH_UNIT ( ) NAMED_UNIT ( * ) SI_UNIT ( .MILLI., .METRE. ) );
#3486=FACE_OUTER_BOUND ( 'NONE', #4481, .T. ) ;
#3489=DIRECTION ( 'NONE',  ( 1.000000000000000000, 0.000000000000000000, 0.000000000000000000 ) ) ;
#3495=CIRCLE ( 'NONE', #2376, 31.52499999999999858 ) ;
#3499=DIRECTION ( 'NONE',  ( 0.000000000000000000, 0.000000000000000000, -1.000000000000000000 ) ) ;
#3526=CARTESIAN_POINT ( 'NONE',  ( 3.499999999999996003, 0.000000000000000000, -35.25000000000000000 ) ) ;
#3546=CARTESIAN_POINT ( 'NONE',  ( -3.500000000000007550, 3.710679801416480038E-15, 30.30000000000000071 ) ) ;
#3566=FACE_OUTER_BOUND ( 'NONE', #4446, .T. ) ;
#3568=ADVANCED_FACE ( 'NONE', ( #3636 ), #3661, .T. ) ;
#3577=DIRECTION ( 'NONE',  ( -1.000000000000000000, 0.000000000000000000, -0.000000000000000000 ) ) ;
#3592=COLOUR_RGB ( '',1.000000000000000000, 0.9490196078431372140, 0.9098039215686274384 ) ;
#3630=DIRECTION ( 'NONE',  ( 0.000000000000000000, 0.000000000000000000, -1.000000000000000000 ) ) ;
#3633=ORIENTED_EDGE ( 'NONE', *, *, #1826, .F. ) ;
#3636=FACE_OUTER_BOUND ( 'NONE', #4117, .T. ) ;
#3639=CARTESIAN_POINT ( 'NONE',  ( 3.499999999999996003, 4.574055794815363937E-15, 37.19999999999999574 ) ) ;
#3646=DIRECTION ( 'NONE',  ( 1.000000000000000000, 0.000000000000000000, 0.000000000000000000 ) ) ;
#3661=TOROIDAL_SURFACE ( 'NONE', #379, 37.19999999999999574, 0.3000000000000007661 ) ;
#3672=CIRCLE ( 'NONE', #5049, 35.97500000000000853 ) ;
#3673=ORIENTED_EDGE ( 'NONE', *, *, #3793, .F. ) ;
#3684=DIRECTION ( 'NONE',  ( 1.000000000000000000, 0.000000000000000000, 0.000000000000000000 ) ) ;
#3689=DIRECTION ( 'NONE',  ( 0.000000000000000000, 0.000000000000000000, 1.000000000000000000 ) ) ;
#3690=FACE_OUTER_BOUND ( 'NONE', #6405, .T. ) ;
#3693=DIRECTION ( 'NONE',  ( -0.000000000000000000, 1.000000000000000000, 1.224646799147353207E-16 ) ) ;
#3695=CARTESIAN_POINT ( 'NONE',  ( -20.63749999999999574, 0.000000000000000000, 0.000000000000000000 ) ) ;
#3697=CARTESIAN_POINT ( 'NONE',  ( -3.199999999999996181, 0.000000000000000000, -37.19999999999999574 ) ) ;
#3704=AXIS2_PLACEMENT_3D ( 'NONE', #5743, #1279, #3689 ) ;
#3707=DIRECTION ( 'NONE',  ( 0.000000000000000000, 0.000000000000000000, -1.000000000000000000 ) ) ;
#3710=ORIENTED_EDGE ( 'NONE', *, *, #4403, .F. ) ;
#3718=FACE_OUTER_BOUND ( 'NONE', #4001, .T. ) ;
#3723=DIRECTION ( 'NONE',  ( 0.000000000000000000, 0.000000000000000000, -1.000000000000000000 ) ) ;
#3726=CARTESIAN_POINT ( 'NONE',  ( -1.677050983124841466, 0.000000000000000000, 0.000000000000000000 ) ) ;
#3755=CIRCLE ( 'NONE', #1103, 30.00000000000000000 ) ;
#3758=DIRECTION ( 'NONE',  ( 0.000000000000000000, 0.000000000000000000, 1.000000000000000000 ) ) ;
#3766=AXIS2_PLACEMENT_3D ( 'NONE', #235, #3795, #5013 ) ;
#3793=EDGE_CURVE ( 'NONE', #3132, #1496, #2178, .T. ) ;
#3795=DIRECTION ( 'NONE',  ( 1.000000000000000000, 0.000000000000000000, 0.000000000000000000 ) ) ;
#3799=AXIS2_PLACEMENT_3D ( 'NONE', #2367, #4757, #5309 ) ;
#3808=DIRECTION ( 'NONE',  ( 1.000000000000000000, 0.000000000000000000, 0.000000000000000000 ) ) ;
#3833=CIRCLE ( 'NONE', #2960, 37.19999999999999574 ) ;
#3836=STYLED_ITEM('',(#7830),#5741);
#3857=VERTEX_POINT ( 'NONE', #3546 ) ;
#3862=CARTESIAN_POINT ( 'NONE',  ( -0.3344772040064616925, 0.000000000000000000, 0.000000000000000000 ) ) ;
#3866=AXIS2_PLACEMENT_3D ( 'NONE', #2930, #3434, #1622 ) ;
#3879=AXIS2_PLACEMENT_3D ( 'NONE', #4197, #6683, #6609 ) ;
#3886=ADVANCED_FACE ( 'NONE', ( #2222 ), #3414, .T. ) ;
#3926=EDGE_LOOP ( 'NONE', ( #2528, #5199, #222, #482 ) ) ;
#3928=CIRCLE ( 'NONE', #3060, 37.50000000000000000 ) ;
#3929=ORIENTED_EDGE ( 'NONE', *, *, #4120, .F. ) ;
#3930=EDGE_CURVE ( 'NONE', #7135, #293, #6941, .T. ) ;
#3966=ORIENTED_EDGE ( 'NONE', *, *, #562, .T. ) ;
#3973=ORIENTED_EDGE ( 'NONE', *, *, #4037, .F. ) ;
#3984=ORIENTED_EDGE ( 'NONE', *, *, #3440, .T. ) ;
#3987=DIRECTION ( 'NONE',  ( 0.000000000000000000, 0.000000000000000000, -1.000000000000000000 ) ) ;
#3996=CARTESIAN_POINT ( 'NONE',  ( 3.200000000000007727, 3.710679801416480038E-15, 30.30000000000000071 ) ) ;
#4001=EDGE_LOOP ( 'NONE', ( #5720, #1441, #6580, #3929 ) ) ;
#4007=DIRECTION ( 'NONE',  ( 0.000000000000000000, 0.000000000000000000, -1.000000000000000000 ) ) ;
#4015=ORIENTED_EDGE ( 'NONE', *, *, #1914, .T. ) ;
#4029=EDGE_CURVE ( 'NONE', #3857, #1907, #3170, .T. ) ;
#4037=EDGE_CURVE ( 'NONE', #7515, #2283, #5804, .T. ) ;
#4039=ORIENTED_EDGE ( 'NONE', *, *, #4403, .T. ) ;
#4043=CARTESIAN_POINT ( 'NONE',  ( -1.677050983124841466, 0.000000000000000000, -32.25000000000000000 ) ) ;
#4049=ORIENTED_EDGE ( 'NONE', *, *, #6490, .F. ) ;
#4058=AXIS2_PLACEMENT_3D ( 'NONE', #199, #2616, #6241 ) ;
#4104=CYLINDRICAL_SURFACE ( 'NONE', #5691, 31.52499999999999858 ) ;
#4105=ORIENTED_EDGE ( 'NONE', *, *, #4384, .T. ) ;
#4107=CIRCLE ( 'NONE', #4742, 0.3000000000000016542 ) ;
#4109=DIRECTION ( 'NONE',  ( 1.000000000000000000, 0.000000000000000000, 0.000000000000000000 ) ) ;
#4117=EDGE_LOOP ( 'NONE', ( #7441, #7091, #2297, #3041 ) ) ;
#4120=EDGE_CURVE ( 'NONE', #4531, #1496, #3672, .T. ) ;
#4123=DIRECTION ( 'NONE',  ( -1.000000000000000000, -0.000000000000000000, -0.000000000000000000 ) ) ;
#4133=DIRECTION ( 'NONE',  ( 1.000000000000000000, 0.000000000000000000, 0.000000000000000000 ) ) ;
#4137=AXIS2_PLACEMENT_3D ( 'NONE', #729, #3577, #6654 ) ;
#4152=DIRECTION ( 'NONE',  ( 0.000000000000000000, 0.000000000000000000, -1.000000000000000000 ) ) ;
#4154=CARTESIAN_POINT ( 'NONE',  ( 3.199999999999996181, 0.000000000000000000, -37.19999999999999574 ) ) ;
#4158=CARTESIAN_POINT ( 'NONE',  ( 3.499999999999996003, 0.000000000000000000, 0.000000000000000000 ) ) ;
#4164=CARTESIAN_POINT ( 'NONE',  ( -3.499999999999996003, 0.000000000000000000, -37.19999999999999574 ) ) ;
#4197=CARTESIAN_POINT ( 'NONE',  ( -3.199999999999994404, 0.000000000000000000, 0.000000000000000000 ) ) ;
#4208=DIRECTION ( 'NONE',  ( 1.000000000000000000, 0.000000000000000000, 0.000000000000000000 ) ) ;
#4215=DIRECTION ( 'NONE',  ( 1.000000000000000000, 0.000000000000000000, 0.000000000000000000 ) ) ;
#4245=CARTESIAN_POINT ( 'NONE',  ( 3.500000000000006661, 0.000000000000000000, 0.000000000000000000 ) ) ;
#4263=CARTESIAN_POINT ( 'NONE',  ( -3.500000000000006661, 3.949485927250214050E-15, 32.25000000000000000 ) ) ;
#4280=DIRECTION ( 'NONE',  ( 0.000000000000000000, 0.000000000000000000, 1.000000000000000000 ) ) ;
#4283=( LENGTH_UNIT ( ) NAMED_UNIT ( * ) SI_UNIT ( .MILLI., .METRE. ) );
#4285=UNCERTAINTY_MEASURE_WITH_UNIT (LENGTH_MEASURE( 1.000000000000000082E-05 ), #3462, 'distance_accuracy_value', 'NONE');
#4289=ORIENTED_EDGE ( 'NONE', *, *, #7213, .F. ) ;
#4291=ORIENTED_EDGE ( 'NONE', *, *, #7359, .F. ) ;
#4292=VECTOR ( 'NONE', #7566, 1000.000000000000000 ) ;
#4295=CARTESIAN_POINT ( 'NONE',  ( -20.63749999999999574, 0.000000000000000000, 0.000000000000000000 ) ) ;
#4305=CYLINDRICAL_SURFACE ( 'NONE', #4616, 32.25000000000000000 ) ;
#4311=ORIENTED_EDGE ( 'NONE', *, *, #5808, .F. ) ;
#4336=CIRCLE ( 'NONE', #552, 0.3000000000000016542 ) ;
#4351=DIRECTION ( 'NONE',  ( 1.000000000000000000, 0.000000000000000000, 0.000000000000000000 ) ) ;
#4381=DIRECTION ( 'NONE',  ( 0.000000000000000000, -1.000000000000000000, 0.000000000000000000 ) ) ;
#4382=EDGE_LOOP ( 'NONE', ( #3085, #2272, #7225, #6249 ) ) ;
#4384=EDGE_CURVE ( 'NONE', #5437, #6698, #6282, .T. ) ;
#4390=ORIENTED_EDGE ( 'NONE', *, *, #6782, .T. ) ;
#4392=CARTESIAN_POINT ( 'NONE',  ( -3.199999999999996181, 0.000000000000000000, 0.000000000000000000 ) ) ;
#4403=EDGE_CURVE ( 'NONE', #1974, #6664, #2393, .T. ) ;
#4415=EDGE_CURVE ( 'NONE', #2423, #719, #2387, .T. ) ;
#4416=ADVANCED_FACE ( 'NONE', ( #3105, #3690 ), #1773, .T. ) ;
#4418=EDGE_CURVE ( 'NONE', #738, #2609, #7293, .T. ) ;
#4423=TOROIDAL_SURFACE ( 'NONE', #3799, 30.30000000000000071, 0.3000000000000003775 ) ;
#4425=TOROIDAL_SURFACE ( 'NONE', #612, 33.75000000000000000, 2.250000000000000444 ) ;
#4446=EDGE_LOOP ( 'NONE', ( #291, #4897 ) ) ;
#4458=AXIS2_PLACEMENT_3D ( 'NONE', #7715, #4208, #66 ) ;
#4464=DIRECTION ( 'NONE',  ( 0.000000000000000000, 0.000000000000000000, 1.000000000000000000 ) ) ;
#4465=FACE_OUTER_BOUND ( 'NONE', #2164, .T. ) ;
#4474=CLOSED_SHELL ( 'NONE', ( #3568, #2989, #5721, #5336, #1419, #862, #2560, #7542, #129, #6537, #6509, #3886, #229, #7282, #605, #7303, #2179, #5247, #471, #187, #1464, #521, #6836, #1144, #7744, #7172, #5092, #4416 ) ) ;
#4481=EDGE_LOOP ( 'NONE', ( #534, #7399, #5472, #5278 ) ) ;
#4498=EDGE_LOOP ( 'NONE', ( #7102, #7466, #7148, #6110 ) ) ;
#4520=ORIENTED_EDGE ( 'NONE', *, *, #7691, .F. ) ;
#4531=VERTEX_POINT ( 'NONE', #6618 ) ;
#4543=DIRECTION ( 'NONE',  ( 0.000000000000000000, 0.000000000000000000, -1.000000000000000000 ) ) ;
#4547=FACE_OUTER_BOUND ( 'NONE', #6035, .T. ) ;
#4553=ORIENTED_EDGE ( 'NONE', *, *, #1184, .F. ) ;
#4561=DIRECTION ( 'NONE',  ( 1.000000000000000000, 0.000000000000000000, 0.000000000000000000 ) ) ;
#4562=CARTESIAN_POINT ( 'NONE',  ( -3.500000000000006661, 0.000000000000000000, 0.000000000000000000 ) ) ;
#4564=FILL_AREA_STYLE_COLOUR ( '', #3592 ) ;
#4574=DIRECTION ( 'NONE',  ( 0.000000000000000000, 0.000000000000000000, -1.000000000000000000 ) ) ;
#4576=AXIS2_PLACEMENT_3D ( 'NONE', #4295, #7298, #3707 ) ;
#4616=AXIS2_PLACEMENT_3D ( 'NONE', #132, #7196, #4902 ) ;
#4624=FACE_OUTER_BOUND ( 'NONE', #5149, .T. ) ;
#4625=EDGE_CURVE ( 'NONE', #5872, #5391, #3383, .T. ) ;
#4630=DIRECTION ( 'NONE',  ( 1.000000000000000000, 0.000000000000000000, 0.000000000000000000 ) ) ;
#4683=EDGE_LOOP ( 'NONE', ( #4105, #1418 ) ) ;
#4697=AXIS2_PLACEMENT_3D ( 'NONE', #3697, #6660, #3071 ) ;
#4713=CIRCLE ( 'NONE', #2202, 35.97500000000000853 ) ;
#4714=ORIENTED_EDGE ( 'NONE', *, *, #4418, .T. ) ;
#4716=FACE_OUTER_BOUND ( 'NONE', #4810, .T. ) ;
#4718=CARTESIAN_POINT ( 'NONE',  ( 3.499999999999996003, 0.000000000000000000, 0.000000000000000000 ) ) ;
#4742=AXIS2_PLACEMENT_3D ( 'NONE', #5840, #6990, #3987 ) ;
#4745=DIRECTION ( 'NONE',  ( 1.000000000000000000, 0.000000000000000000, 0.000000000000000000 ) ) ;
#4756=VECTOR ( 'NONE', #3646, 1000.000000000000000 ) ;
#4757=DIRECTION ( 'NONE',  ( 1.000000000000000000, 0.000000000000000000, 0.000000000000000000 ) ) ;
#4758=EDGE_CURVE ( 'NONE', #1496, #147, #5276, .T. ) ;
#4764=ORIENTED_EDGE ( 'NONE', *, *, #895, .T. ) ;
#4810=EDGE_LOOP ( 'NONE', ( #4015, #2392, #34, #7 ) ) ;
#4818=ORIENTED_EDGE ( 'NONE', *, *, #5446, .T. ) ;
#4828=DIRECTION ( 'NONE',  ( 1.000000000000000000, 0.000000000000000000, 0.000000000000000000 ) ) ;
#4870=CARTESIAN_POINT ( 'NONE',  ( -3.500000000000007105, 32.25000000000000000, 0.000000000000000000 ) ) ;
#4887=EDGE_LOOP ( 'NONE', ( #69, #4714, #3007, #3633 ) ) ;
#4897=ORIENTED_EDGE ( 'NONE', *, *, #4037, .T. ) ;
#4902=DIRECTION ( 'NONE',  ( 0.000000000000000000, 0.000000000000000000, -1.000000000000000000 ) ) ;
#4905=CARTESIAN_POINT ( 'NONE',  ( -20.63749999999999574, 0.000000000000000000, -37.50000000000000000 ) ) ;
#4907=CIRCLE ( 'NONE', #5535, 32.25000000000000000 ) ;
#4913=DIRECTION ( 'NONE',  ( -1.000000000000000000, -0.000000000000000000, -0.000000000000000000 ) ) ;
#4927=ORIENTED_EDGE ( 'NONE', *, *, #982, .T. ) ;
#4934=AXIS2_PLACEMENT_3D ( 'NONE', #5845, #2153, #4543 ) ;
#4937=DIRECTION ( 'NONE',  ( 0.000000000000000000, 0.000000000000000000, -1.000000000000000000 ) ) ;
#4943=DIRECTION ( 'NONE',  ( 1.000000000000000000, 0.000000000000000000, 0.000000000000000000 ) ) ;
#4944=ORIENTED_EDGE ( 'NONE', *, *, #6164, .T. ) ;
#4946=DIRECTION ( 'NONE',  ( 0.000000000000000000, 0.000000000000000000, 1.000000000000000000 ) ) ;
#4963=CARTESIAN_POINT ( 'NONE',  ( -3.199999999999994404, 4.592425496802574367E-15, 37.50000000000000000 ) ) ;
#4973=DIRECTION ( 'NONE',  ( 1.000000000000000000, 0.000000000000000000, 0.000000000000000000 ) ) ;
#4987=FACE_OUTER_BOUND ( 'NONE', #7055, .T. ) ;
#4991=AXIS2_PLACEMENT_3D ( 'NONE', #834, #7460, #4464 ) ;
#5006=ORIENTED_EDGE ( 'NONE', *, *, #6253, .T. ) ;
#5013=DIRECTION ( 'NONE',  ( 0.000000000000000000, 0.000000000000000000, -1.000000000000000000 ) ) ;
#5018=FACE_OUTER_BOUND ( 'NONE', #7271, .T. ) ;
#5033=ORIENTED_EDGE ( 'NONE', *, *, #5446, .F. ) ;
#5045=AXIS2_PLACEMENT_3D ( 'NONE', #975, #1613, #7056 ) ;
#5049=AXIS2_PLACEMENT_3D ( 'NONE', #3862, #1448, #5666 ) ;
#5079=AXIS2_PLACEMENT_3D ( 'NONE', #3197, #2533, #2421 ) ;
#5083=CARTESIAN_POINT ( 'NONE',  ( 0.000000000000000000, 0.000000000000000000, 33.75000000000000000 ) ) ;
#5085=DIRECTION ( 'NONE',  ( 0.000000000000000000, 0.000000000000000000, -1.000000000000000000 ) ) ;
#5092=ADVANCED_FACE ( 'NONE', ( #6765, #5533 ), #2805, .T. ) ;
#5093=CARTESIAN_POINT ( 'NONE',  ( 3.199999999999994404, 4.592425496802574367E-15, 37.50000000000000000 ) ) ;
#5095=DIRECTION ( 'NONE',  ( 0.000000000000000000, 0.000000000000000000, -1.000000000000000000 ) ) ;
#5109=ORIENTED_EDGE ( 'NONE', *, *, #6848, .T. ) ;
#5127=CIRCLE ( 'NONE', #3879, 37.50000000000000000 ) ;
#5131=FACE_OUTER_BOUND ( 'NONE', #6531, .T. ) ;
#5148=ORIENTED_EDGE ( 'NONE', *, *, #2507, .T. ) ;
#5149=EDGE_LOOP ( 'NONE', ( #4039, #5148, #78, #184 ) ) ;
#5150=AXIS2_PLACEMENT_3D ( 'NONE', #401, #7074, #5773 ) ;
#5154=CARTESIAN_POINT ( 'NONE',  ( -3.200000000000008171, 0.000000000000000000, -30.00000000000000000 ) ) ;
#5161=CARTESIAN_POINT ( 'NONE',  ( -20.63749999999999574, 0.000000000000000000, -35.97500000000000853 ) ) ;
#5184=ORIENTED_EDGE ( 'NONE', *, *, #905, .F. ) ;
#5186=AXIS2_PLACEMENT_3D ( 'NONE', #1844, #3684, #6095 ) ;
#5189=CARTESIAN_POINT ( 'NONE',  ( -20.63749999999999929, 3.673940397442059178E-15, 30.00000000000000000 ) ) ;
#5196=CYLINDRICAL_SURFACE ( 'NONE', #5962, 31.52499999999999858 ) ;
#5199=ORIENTED_EDGE ( 'NONE', *, *, #2929, .T. ) ;
#5227=ORIENTED_EDGE ( 'NONE', *, *, #280, .T. ) ;
#5233=DIRECTION ( 'NONE',  ( 1.000000000000000000, 0.000000000000000000, 0.000000000000000000 ) ) ;
#5247=ADVANCED_FACE ( 'NONE', ( #5958 ), #2344, .F. ) ;
#5252=CARTESIAN_POINT ( 'NONE',  ( 0.000000000000000000, 0.000000000000000000, 33.75000000000000000 ) ) ;
#5269=AXIS2_PLACEMENT_3D ( 'NONE', #2443, #6726, #1919 ) ;
#5276=CIRCLE ( 'NONE', #5150, 2.250000000000001776 ) ;
#5278=ORIENTED_EDGE ( 'NONE', *, *, #3930, .T. ) ;
#5309=DIRECTION ( 'NONE',  ( 0.000000000000000000, 0.000000000000000000, -1.000000000000000000 ) ) ;
#5325=EDGE_LOOP ( 'NONE', ( #4049, #1094, #3966, #3973 ) ) ;
#5336=ADVANCED_FACE ( 'NONE', ( #7222 ), #6667, .F. ) ;
#5356=FACE_OUTER_BOUND ( 'NONE', #5565, .T. ) ;
#5367=DIRECTION ( 'NONE',  ( 0.000000000000000000, 0.000000000000000000, -1.000000000000000000 ) ) ;
#5369=AXIS2_PLACEMENT_3D ( 'NONE', #2001, #5690, #7392 ) ;
#5377=VERTEX_POINT ( 'NONE', #152 ) ;
#5385=DIRECTION ( 'NONE',  ( 1.000000000000000000, 0.000000000000000000, 0.000000000000000000 ) ) ;
#5391=VERTEX_POINT ( 'NONE', #4963 ) ;
#5403=AXIS2_PLACEMENT_3D ( 'NONE', #6333, #769, #6217 ) ;
#5407=LINE ( 'NONE', #5954, #6044 ) ;
#5411=EDGE_LOOP ( 'NONE', ( #2546, #867, #4311, #2647 ) ) ;
#5417=ORIENTED_EDGE ( 'NONE', *, *, #4120, .T. ) ;
#5437=VERTEX_POINT ( 'NONE', #6789 ) ;
#5446=EDGE_CURVE ( 'NONE', #2154, #3231, #7230, .T. ) ;
#5455=LINE ( 'NONE', #6645, #1213 ) ;
#5469=DIRECTION ( 'NONE',  ( 1.000000000000000000, 0.000000000000000000, 0.000000000000000000 ) ) ;
#5472=ORIENTED_EDGE ( 'NONE', *, *, #5916, .T. ) ;
#5492=TOROIDAL_SURFACE ( 'NONE', #4991, 33.75000000000000000, 2.250000000000000444 ) ;
#5500=DIRECTION ( 'NONE',  ( -0.000000000000000000, 0.000000000000000000, 1.000000000000000000 ) ) ;
#5501=CIRCLE ( 'NONE', #7141, 37.19999999999999574 ) ;
#5532=DIRECTION ( 'NONE',  ( 0.000000000000000000, 0.000000000000000000, -1.000000000000000000 ) ) ;
#5533=FACE_BOUND ( 'NONE', #7718, .T. ) ;
#5535=AXIS2_PLACEMENT_3D ( 'NONE', #3069, #145, #7287 ) ;
#5565=EDGE_LOOP ( 'NONE', ( #1180, #2611, #6994, #4944 ) ) ;
#5589=CARTESIAN_POINT ( 'NONE',  ( -20.63749999999999574, 4.316879966994420283E-15, 35.25000000000000000 ) ) ;
#5605=MECHANICAL_DESIGN_GEOMETRIC_PRESENTATION_REPRESENTATION('',(#3836),#6739);
#5607=FACE_OUTER_BOUND ( 'NONE', #4498, .T. ) ;
#5616=ORIENTED_EDGE ( 'NONE', *, *, #2068, .F. ) ;
#5619=DIRECTION ( 'NONE',  ( 0.000000000000000000, 0.000000000000000000, -1.000000000000000000 ) ) ;
#5625=CIRCLE ( 'NONE', #2236, 30.30000000000000071 ) ;
#5643=CARTESIAN_POINT ( 'NONE',  ( 3.200000000000008171, 0.000000000000000000, -30.00000000000000000 ) ) ;
#5644=VERTEX_POINT ( 'NONE', #5946 ) ;
#5666=DIRECTION ( 'NONE',  ( 0.000000000000000000, 0.000000000000000000, -1.000000000000000000 ) ) ;
#5668=( NAMED_UNIT ( * ) PLANE_ANGLE_UNIT ( ) SI_UNIT ( $, .RADIAN. ) );
#5678=EDGE_CURVE ( 'NONE', #3132, #7232, #1949, .T. ) ;
#5686=DIRECTION ( 'NONE',  ( 1.000000000000000000, 0.000000000000000000, 0.000000000000000000 ) ) ;
#5690=DIRECTION ( 'NONE',  ( 1.000000000000000000, 0.000000000000000000, 0.000000000000000000 ) ) ;
#5691=AXIS2_PLACEMENT_3D ( 'NONE', #1665, #321, #2775 ) ;
#5705=CIRCLE ( 'NONE', #3196, 30.00000000000000000 ) ;
#5720=ORIENTED_EDGE ( 'NONE', *, *, #3129, .F. ) ;
#5721=ADVANCED_FACE ( 'NONE', ( #2836 ), #3204, .T. ) ;
#5729=MECHANICAL_DESIGN_GEOMETRIC_PRESENTATION_REPRESENTATION('',(#6867),#7745);
#5737=LINE ( 'NONE', #6184, #564 ) ;
#5741=MANIFOLD_SOLID_BREP ( 'OuterRace', #4474 ) ;
#5743=CARTESIAN_POINT ( 'NONE',  ( 1.677050983124841466, 0.000000000000000000, 0.000000000000000000 ) ) ;
#5766=EDGE_CURVE ( 'NONE', #1095, #2423, #2708, .T. ) ;
#5773=DIRECTION ( 'NONE',  ( 0.000000000000000000, -1.224646799147352961E-16, 1.000000000000000000 ) ) ;
#5804=CIRCLE ( 'NONE', #6822, 31.52499999999999858 ) ;
#5808=EDGE_CURVE ( 'NONE', #2283, #7515, #807, .T. ) ;
#5839=ORIENTED_EDGE ( 'NONE', *, *, #2068, .T. ) ;
#5840=CARTESIAN_POINT ( 'NONE',  ( 3.200000000000007727, 0.000000000000000000, -30.30000000000000071 ) ) ;
#5845=CARTESIAN_POINT ( 'NONE',  ( -20.63749999999999929, 0.000000000000000000, 0.000000000000000000 ) ) ;
#5872=VERTEX_POINT ( 'NONE', #1399 ) ;
#5879=ORIENTED_EDGE ( 'NONE', *, *, #2025, .F. ) ;
#5916=EDGE_CURVE ( 'NONE', #2423, #7135, #5737, .T. ) ;
#5937=CARTESIAN_POINT ( 'NONE',  ( 3.200000000000008171, 0.000000000000000000, 0.000000000000000000 ) ) ;
#5946=CARTESIAN_POINT ( 'NONE',  ( -3.199999999999994404, 0.000000000000000000, -37.50000000000000000 ) ) ;
#5950=VERTEX_POINT ( 'NONE', #6415 ) ;
#5951=AXIS2_PLACEMENT_3D ( 'NONE', #4870, #6725, #5500 ) ;
#5954=CARTESIAN_POINT ( 'NONE',  ( -20.63749999999999574, 4.405666859932604686E-15, 35.97500000000000853 ) ) ;
#5958=FACE_OUTER_BOUND ( 'NONE', #2270, .T. ) ;
#5962=AXIS2_PLACEMENT_3D ( 'NONE', #1762, #2207, #4152 ) ;
#5977=DIRECTION ( 'NONE',  ( 1.000000000000000000, 0.000000000000000000, 0.000000000000000000 ) ) ;
#5995=ORIENTED_EDGE ( 'NONE', *, *, #7071, .F. ) ;
#6000=ORIENTED_EDGE ( 'NONE', *, *, #7359, .T. ) ;
#6020=ORIENTED_EDGE ( 'NONE', *, *, #616, .T. ) ;
#6035=EDGE_LOOP ( 'NONE', ( #5184, #661, #7671, #650 ) ) ;
#6037=ORIENTED_EDGE ( 'NONE', *, *, #601, .T. ) ;
#6038=CARTESIAN_POINT ( 'NONE',  ( 3.500000000000006661, 0.000000000000000000, 0.000000000000000000 ) ) ;
#6044=VECTOR ( 'NONE', #4215, 1000.000000000000000 ) ;
#6064=DIRECTION ( 'NONE',  ( -1.000000000000000000, -0.000000000000000000, -0.000000000000000000 ) ) ;
#6089=DIRECTION ( 'NONE',  ( 0.000000000000000000, 1.000000000000000000, -1.224646799147353207E-16 ) ) ;
#6095=DIRECTION ( 'NONE',  ( 0.000000000000000000, 0.000000000000000000, -1.000000000000000000 ) ) ;
#6097=CARTESIAN_POINT ( 'NONE',  ( 3.499999999999996003, 4.316879966994419494E-15, 35.25000000000000000 ) ) ;
#6101=AXIS2_PLACEMENT_3D ( 'NONE', #7755, #2291, #2956 ) ;
#6110=ORIENTED_EDGE ( 'NONE', *, *, #6753, .F. ) ;
#6116=( GEOMETRIC_REPRESENTATION_CONTEXT ( 3 ) GLOBAL_UNCERTAINTY_ASSIGNED_CONTEXT ( ( #6754 ) ) GLOBAL_UNIT_ASSIGNED_CONTEXT ( ( #7406, #5668, #741 ) ) REPRESENTATION_CONTEXT ( 'NONE', 'WORKASPACE' ) );
#6121=DIRECTION ( 'NONE',  ( 0.000000000000000000, 0.000000000000000000, -1.000000000000000000 ) ) ;
#6122=DIRECTION ( 'NONE',  ( 0.000000000000000000, -1.000000000000000000, 0.000000000000000000 ) ) ;
#6135=DIRECTION ( 'NONE',  ( 0.000000000000000000, 0.000000000000000000, -1.000000000000000000 ) ) ;
#6136=ORIENTED_EDGE ( 'NONE', *, *, #5678, .T. ) ;
#6161=EDGE_CURVE ( 'NONE', #293, #7135, #60, .T. ) ;
#6164=EDGE_CURVE ( 'NONE', #688, #147, #3214, .T. ) ;
#6176=ORIENTED_EDGE ( 'NONE', *, *, #1914, .F. ) ;
#6184=CARTESIAN_POINT ( 'NONE',  ( -20.63749999999999574, 0.000000000000000000, -35.25000000000000000 ) ) ;
#6217=DIRECTION ( 'NONE',  ( 0.000000000000000000, 1.224646799147359124E-16, 1.000000000000000000 ) ) ;
#6224=ORIENTED_EDGE ( 'NONE', *, *, #6753, .T. ) ;
#6241=DIRECTION ( 'NONE',  ( 0.000000000000000000, 0.000000000000000000, -1.000000000000000000 ) ) ;
#6249=ORIENTED_EDGE ( 'NONE', *, *, #2628, .F. ) ;
#6253=EDGE_CURVE ( 'NONE', #1907, #3857, #273, .T. ) ;
#6256=PRODUCT_CONTEXT ( 'NONE', #6915, 'mechanical' ) ;
#6270=EDGE_CURVE ( 'NONE', #5391, #5644, #153, .T. ) ;
#6282=CIRCLE ( 'NONE', #978, 37.19999999999999574 ) ;
#6298=ORIENTED_EDGE ( 'NONE', *, *, #4758, .T. ) ;
#6325=DIRECTION ( 'NONE',  ( 1.000000000000000000, 0.000000000000000000, 0.000000000000000000 ) ) ;
#6329=DIRECTION ( 'NONE',  ( 0.000000000000000000, 0.000000000000000000, -1.000000000000000000 ) ) ;
#6333=CARTESIAN_POINT ( 'NONE',  ( -3.199999999999996181, 4.555686092828153507E-15, 37.19999999999999574 ) ) ;
#6398=EDGE_CURVE ( 'NONE', #2609, #738, #3928, .T. ) ;
#6404=LINE ( 'NONE', #2311, #6453 ) ;
#6405=EDGE_LOOP ( 'NONE', ( #4553, #4291 ) ) ;
#6415=CARTESIAN_POINT ( 'NONE',  ( 3.200000000000008171, 3.692310099429270397E-15, 30.00000000000000000 ) ) ;
#6453=VECTOR ( 'NONE', #2233, 1000.000000000000000 ) ;
#6470=EDGE_LOOP ( 'NONE', ( #5006, #7438 ) ) ;
#6471=DIRECTION ( 'NONE',  ( 0.000000000000000000, 0.000000000000000000, -1.000000000000000000 ) ) ;
#6483=CARTESIAN_POINT ( 'NONE',  ( -20.63749999999999929, 0.000000000000000000, -31.52499999999999858 ) ) ;
#6490=EDGE_CURVE ( 'NONE', #5377, #7515, #6404, .T. ) ;
#6499=SURFACE_SIDE_STYLE ('',( #3386 ) ) ;
#6509=ADVANCED_FACE ( 'NONE', ( #7536 ), #4104, .T. ) ;
#6510=CARTESIAN_POINT ( 'NONE',  ( -20.63749999999999929, 0.000000000000000000, 0.000000000000000000 ) ) ;
#6525=CIRCLE ( 'NONE', #1996, 37.19999999999999574 ) ;
#6531=EDGE_LOOP ( 'NONE', ( #4520, #6020, #4927, #4289 ) ) ;
#6537=ADVANCED_FACE ( 'NONE', ( #4624 ), #3404, .T. ) ;
#6565=DIRECTION ( 'NONE',  ( 0.000000000000000000, 0.000000000000000000, -1.000000000000000000 ) ) ;
#6569=DIRECTION ( 'NONE',  ( 1.000000000000000000, 0.000000000000000000, 0.000000000000000000 ) ) ;
#6580=ORIENTED_EDGE ( 'NONE', *, *, #3793, .T. ) ;
#6606=DIRECTION ( 'NONE',  ( 0.000000000000000000, 1.224646799147359124E-16, 1.000000000000000000 ) ) ;
#6607=CARTESIAN_POINT ( 'NONE',  ( 3.199999999999996181, 0.000000000000000000, 0.000000000000000000 ) ) ;
#6609=DIRECTION ( 'NONE',  ( 0.000000000000000000, 0.000000000000000000, -1.000000000000000000 ) ) ;
#6616=FACE_OUTER_BOUND ( 'NONE', #1253, .T. ) ;
#6618=CARTESIAN_POINT ( 'NONE',  ( -0.3344772040064616925, 0.000000000000000000, 35.97500000000000853 ) ) ;
#6619=FACE_OUTER_BOUND ( 'NONE', #3926, .T. ) ;
#6629=CARTESIAN_POINT ( 'NONE',  ( -3.499999999999996003, 0.000000000000000000, -35.97500000000000142 ) ) ;
#6633=ORIENTED_EDGE ( 'NONE', *, *, #3129, .T. ) ;
#6641=EDGE_CURVE ( 'NONE', #738, #6698, #6956, .T. ) ;
#6645=CARTESIAN_POINT ( 'NONE',  ( -20.63749999999999929, 0.000000000000000000, -30.00000000000000000 ) ) ;
#6654=DIRECTION ( 'NONE',  ( -0.000000000000000000, 0.000000000000000000, 1.000000000000000000 ) ) ;
#6657=DIRECTION ( 'NONE',  ( 1.000000000000000000, 0.000000000000000000, 0.000000000000000000 ) ) ;
#6660=DIRECTION ( 'NONE',  ( 0.000000000000000000, -1.000000000000000000, 0.000000000000000000 ) ) ;
#6664=VERTEX_POINT ( 'NONE', #4263 ) ;
#6667=CYLINDRICAL_SURFACE ( 'NONE', #4576, 35.97500000000000853 ) ;
#6673=CARTESIAN_POINT ( 'NONE',  ( -20.63749999999999929, 3.949485927250214050E-15, 32.25000000000000000 ) ) ;
#6683=DIRECTION ( 'NONE',  ( 1.000000000000000000, 0.000000000000000000, 0.000000000000000000 ) ) ;
#6691=CARTESIAN_POINT ( 'NONE',  ( 3.199999999999994404, 0.000000000000000000, 0.000000000000000000 ) ) ;
#6698=VERTEX_POINT ( 'NONE', #3639 ) ;
#6706=EDGE_LOOP ( 'NONE', ( #5839, #432, #3426, #5879 ) ) ;
#6721=DIRECTION ( 'NONE',  ( 0.000000000000000000, 0.000000000000000000, -1.000000000000000000 ) ) ;
#6725=DIRECTION ( 'NONE',  ( -1.000000000000000000, 0.000000000000000000, -0.000000000000000000 ) ) ;
#6726=DIRECTION ( 'NONE',  ( 1.000000000000000000, 0.000000000000000000, 0.000000000000000000 ) ) ;
#6731=CARTESIAN_POINT ( 'NONE',  ( 0.000000000000000000, 4.133182947122317561E-15, -33.75000000000000000 ) ) ;
#6739=( GEOMETRIC_REPRESENTATION_CONTEXT ( 3 ) GLOBAL_UNCERTAINTY_ASSIGNED_CONTEXT ( ( #2514 ) ) GLOBAL_UNIT_ASSIGNED_CONTEXT ( ( #4283, #1284, #1209 ) ) REPRESENTATION_CONTEXT ( 'NONE', 'WORKASPACE' ) );
#6753=EDGE_CURVE ( 'NONE', #3231, #1907, #7578, .T. ) ;
#6754=UNCERTAINTY_MEASURE_WITH_UNIT (LENGTH_MEASURE( 1.000000000000000082E-05 ), #7406, 'distance_accuracy_value', 'NONE');
#6764=CARTESIAN_POINT ( 'NONE',  ( -0.3344772040064616925, 0.000000000000000000, 0.000000000000000000 ) ) ;
#6765=FACE_OUTER_BOUND ( 'NONE', #4683, .T. ) ;
#6782=EDGE_CURVE ( 'NONE', #1974, #147, #7420, .T. ) ;
#6789=CARTESIAN_POINT ( 'NONE',  ( 3.499999999999996003, 0.000000000000000000, -37.19999999999999574 ) ) ;
#6794=VERTEX_POINT ( 'NONE', #5643 ) ;
#6799=CARTESIAN_POINT ( 'NONE',  ( -20.63749999999999929, 0.000000000000000000, -32.25000000000000000 ) ) ;
#6803=PLANE ( 'NONE',  #1813 ) ;
#6820=ORIENTED_EDGE ( 'NONE', *, *, #2628, .T. ) ;
#6822=AXIS2_PLACEMENT_3D ( 'NONE', #6038, #3077, #1894 ) ;
#6836=ADVANCED_FACE ( 'NONE', ( #3718 ), #2654, .F. ) ;
#6848=EDGE_CURVE ( 'NONE', #7232, #3132, #3432, .T. ) ;
#6867=STYLED_ITEM ( 'NONE', ( #2289 ), #1052 ) ;
#6915=APPLICATION_CONTEXT ( 'automotive_design' ) ;
#6941=CIRCLE ( 'NONE', #2660, 35.25000000000000000 ) ;
#6952=AXIS2_PLACEMENT_3D ( 'NONE', #3251, #4351, #3213 ) ;
#6956=CIRCLE ( 'NONE', #782, 0.3000000000000016542 ) ;
#6973=( NAMED_UNIT ( * ) SI_UNIT ( $, .STERADIAN. ) SOLID_ANGLE_UNIT ( ) );
#6990=DIRECTION ( 'NONE',  ( 0.000000000000000000, -1.000000000000000000, 0.000000000000000000 ) ) ;
#6994=ORIENTED_EDGE ( 'NONE', *, *, #997, .T. ) ;
#7003=VERTEX_POINT ( 'NONE', #1852 ) ;
#7004=ORIENTED_EDGE ( 'NONE', *, *, #6848, .F. ) ;
#7015=ORIENTED_EDGE ( 'NONE', *, *, #6164, .F. ) ;
#7044=VERTEX_POINT ( 'NONE', #1286 ) ;
#7052=CARTESIAN_POINT ( 'NONE',  ( 3.199999999999994404, 0.000000000000000000, -37.50000000000000000 ) ) ;
#7055=EDGE_LOOP ( 'NONE', ( #343, #4818, #6224, #2494 ) ) ;
#7056=DIRECTION ( 'NONE',  ( 0.000000000000000000, 0.000000000000000000, 1.000000000000000000 ) ) ;
#7059=PRODUCT_DEFINITION ( 'UNKNOWN', '', #7221, #1456 ) ;
#7071=EDGE_CURVE ( 'NONE', #1401, #5644, #1299, .T. ) ;
#7074=DIRECTION ( 'NONE',  ( -0.000000000000000000, 1.000000000000000000, 1.224646799147353207E-16 ) ) ;
#7091=ORIENTED_EDGE ( 'NONE', *, *, #6641, .T. ) ;
#7102=ORIENTED_EDGE ( 'NONE', *, *, #1869, .T. ) ;
#7128=DIRECTION ( 'NONE',  ( 1.000000000000000000, 0.000000000000000000, 0.000000000000000000 ) ) ;
#7135=VERTEX_POINT ( 'NONE', #3526 ) ;
#7141=AXIS2_PLACEMENT_3D ( 'NONE', #7502, #3217, #6329 ) ;
#7148=ORIENTED_EDGE ( 'NONE', *, *, #6253, .F. ) ;
#7149=AXIS2_PLACEMENT_3D ( 'NONE', #996, #3489, #2861 ) ;
#7172=ADVANCED_FACE ( 'NONE', ( #1113 ), #283, .T. ) ;
#7195=AXIS2_PLACEMENT_3D ( 'NONE', #2418, #3117, #3630 ) ;
#7196=DIRECTION ( 'NONE',  ( 1.000000000000000000, 0.000000000000000000, 0.000000000000000000 ) ) ;
#7213=EDGE_CURVE ( 'NONE', #5950, #6794, #5705, .T. ) ;
#7221=PRODUCT_DEFINITION_FORMATION_WITH_SPECIFIED_SOURCE ( 'ANY', '', #7248, .NOT_KNOWN. ) ;
#7222=FACE_OUTER_BOUND ( 'NONE', #1805, .T. ) ;
#7225=ORIENTED_EDGE ( 'NONE', *, *, #4415, .T. ) ;
#7228=EDGE_CURVE ( 'NONE', #2154, #5950, #2754, .T. ) ;
#7229=DIRECTION ( 'NONE',  ( 1.000000000000000000, 0.000000000000000000, 0.000000000000000000 ) ) ;
#7230=CIRCLE ( 'NONE', #5079, 30.00000000000000000 ) ;
#7232=VERTEX_POINT ( 'NONE', #2433 ) ;
#7248=PRODUCT ( 'angular contact ball bearing_68_iso_ISO 15 ABB - 1760 - 38,SI,NC,38_68', 'angular contact ball bearing_68_iso_ISO 15 ABB - 1760 - 38,SI,NC,38_68', '', ( #6256 ) ) ;
#7254=EDGE_LOOP ( 'NONE', ( #937, #3984, #6820, #5227 ) ) ;
#7255=ORIENTED_EDGE ( 'NONE', *, *, #7401, .F. ) ;
#7265=CIRCLE ( 'NONE', #3866, 32.25000000000000000 ) ;
#7271=EDGE_LOOP ( 'NONE', ( #5417, #6298, #2165, #7487 ) ) ;
#7282=ADVANCED_FACE ( 'NONE', ( #2169 ), #5196, .T. ) ;
#7287=DIRECTION ( 'NONE',  ( 0.000000000000000000, 0.000000000000000000, -1.000000000000000000 ) ) ;
#7290=AXIS2_PLACEMENT_3D ( 'NONE', #3249, #6325, #5095 ) ;
#7293=CIRCLE ( 'NONE', #2261, 37.50000000000000000 ) ;
#7298=DIRECTION ( 'NONE',  ( 1.000000000000000000, 0.000000000000000000, 0.000000000000000000 ) ) ;
#7302=AXIS2_PLACEMENT_3D ( 'NONE', #3695, #2006, #2524 ) ;
#7303=ADVANCED_FACE ( 'NONE', ( #3566, #2396 ), #6803, .T. ) ;
#7329=LINE ( 'NONE', #5589, #868 ) ;
#7359=EDGE_CURVE ( 'NONE', #5872, #1401, #3833, .T. ) ;
#7380=DIRECTION ( 'NONE',  ( 0.000000000000000000, -1.000000000000000000, 0.000000000000000000 ) ) ;
#7392=DIRECTION ( 'NONE',  ( 0.000000000000000000, 0.000000000000000000, -1.000000000000000000 ) ) ;
#7397=CYLINDRICAL_SURFACE ( 'NONE', #7302, 37.50000000000000000 ) ;
#7399=ORIENTED_EDGE ( 'NONE', *, *, #4415, .F. ) ;
#7401=EDGE_CURVE ( 'NONE', #1496, #4531, #4713, .T. ) ;
#7406=( LENGTH_UNIT ( ) NAMED_UNIT ( * ) SI_UNIT ( .MILLI., .METRE. ) );
#7420=LINE ( 'NONE', #6799, #2808 ) ;
#7429=CARTESIAN_POINT ( 'NONE',  ( 0.3344772040064616925, 4.088789500653224965E-15, -31.52499999999999858 ) ) ;
#7438=ORIENTED_EDGE ( 'NONE', *, *, #4029, .T. ) ;
#7441=ORIENTED_EDGE ( 'NONE', *, *, #6398, .T. ) ;
#7460=DIRECTION ( 'NONE',  ( -1.000000000000000000, -0.000000000000000000, -0.000000000000000000 ) ) ;
#7463=AXIS2_PLACEMENT_3D ( 'NONE', #1990, #4381, #1416 ) ;
#7466=ORIENTED_EDGE ( 'NONE', *, *, #565, .T. ) ;
#7485=AXIS2_PLACEMENT_3D ( 'NONE', #1301, #3758, #5977 ) ;
#7487=ORIENTED_EDGE ( 'NONE', *, *, #997, .F. ) ;
#7502=CARTESIAN_POINT ( 'NONE',  ( -3.499999999999996003, 0.000000000000000000, 0.000000000000000000 ) ) ;
#7504=DIRECTION ( 'NONE',  ( 0.000000000000000000, 1.224646799147359124E-16, 1.000000000000000000 ) ) ;
#7515=VERTEX_POINT ( 'NONE', #2187 ) ;
#7523=ORIENTED_EDGE ( 'NONE', *, *, #4625, .F. ) ;
#7536=FACE_OUTER_BOUND ( 'NONE', #5411, .T. ) ;
#7542=ADVANCED_FACE ( 'NONE', ( #4465 ), #908, .F. ) ;
#7559=AXIS2_PLACEMENT_3D ( 'NONE', #435, #2931, #2850 ) ;
#7566=DIRECTION ( 'NONE',  ( 1.000000000000000000, 0.000000000000000000, 0.000000000000000000 ) ) ;
#7578=CIRCLE ( 'NONE', #7463, 0.3000000000000016542 ) ;
#7585=EDGE_LOOP ( 'NONE', ( #7523, #6000, #1872, #1740 ) ) ;
#7596=AXIS2_PLACEMENT_3D ( 'NONE', #6510, #549, #5367 ) ;
#7607=AXIS2_PLACEMENT_3D ( 'NONE', #4245, #6657, #1247 ) ;
#7610=ORIENTED_EDGE ( 'NONE', *, *, #1869, .F. ) ;
#7612=AXIS2_PLACEMENT_3D ( 'NONE', #3726, #4828, #6135 ) ;
#7623=DIRECTION ( 'NONE',  ( 0.000000000000000000, 1.000000000000000000, -1.224646799147353207E-16 ) ) ;
#7636=SHAPE_REPRESENTATION_RELATIONSHIP ( 'NONE' , 'NONE' ,  #420, #1052 ) ;
#7645=TOROIDAL_SURFACE ( 'NONE', #1739, 33.75000000000000000, 2.250000000000000444 ) ;
#7666=AXIS2_PLACEMENT_3D ( 'NONE', #2551, #902, #4574 ) ;
#7671=ORIENTED_EDGE ( 'NONE', *, *, #2025, .T. ) ;
#7683=CARTESIAN_POINT ( 'NONE',  ( 3.499999999999996003, 0.000000000000000000, 0.000000000000000000 ) ) ;
#7691=EDGE_CURVE ( 'NONE', #7044, #5950, #4336, .T. ) ;
#7700=EDGE_LOOP ( 'NONE', ( #6136, #5109 ) ) ;
#7715=CARTESIAN_POINT ( 'NONE',  ( -3.199999999999996181, 0.000000000000000000, 0.000000000000000000 ) ) ;
#7718=EDGE_LOOP ( 'NONE', ( #313, #563 ) ) ;
#7739=DIRECTION ( 'NONE',  ( 0.000000000000000000, 0.000000000000000000, -1.000000000000000000 ) ) ;
#7742=CARTESIAN_POINT ( 'NONE',  ( 3.500000000000006661, 0.000000000000000000, 0.000000000000000000 ) ) ;
#7744=ADVANCED_FACE ( 'NONE', ( #4547 ), #3409, .T. ) ;
#7745=( GEOMETRIC_REPRESENTATION_CONTEXT ( 3 ) GLOBAL_UNCERTAINTY_ASSIGNED_CONTEXT ( ( #4285 ) ) GLOBAL_UNIT_ASSIGNED_CONTEXT ( ( #3462, #2872, #6973 ) ) REPRESENTATION_CONTEXT ( 'NONE', 'WORKASPACE' ) );
#7755=CARTESIAN_POINT ( 'NONE',  ( -3.499999999999996003, 0.000000000000000000, 0.000000000000000000 ) ) ;
#7824=COLOUR_RGB('Grey',0.48,0.52,0.57);
#7825=FILL_AREA_STYLE_COLOUR('',#7824);
#7826=FILL_AREA_STYLE('',(#7825));
#7827=SURFACE_STYLE_FILL_AREA(#7826);
#7828=SURFACE_SIDE_STYLE('',(#7827));
#7829=SURFACE_STYLE_USAGE(.BOTH.,#7828);
#7830=PRESENTATION_STYLE_ASSIGNMENT((#7829));
ENDSEC;
END-ISO-10303-21;
